ISO-10303-21;
HEADER;
/* Generated by software containing ST-Developer
 * from STEP Tools, Inc. (www.steptools.com) 
 */

FILE_DESCRIPTION(
/* description */ ('STEP AP214', 'CAx-IF Rec.Pracs.---Representation and Presentation of Product Manufa
cturing Information (PMI)---4.0---2014-10-13'),
/* implementation_level */ '2;1');

FILE_NAME(
/* name */ 'Release Valve Screw.step',
/* time_stamp */ '2026-10-28T23:34:22+01:00',
/* author */ (''),
/* organization */ (''),
/* preprocessor_version */ 'ST-DEVELOPER v20.2',
/* originating_system */ 'Autodesk Translation Framework v15.17.0.0',
/* authorisation */ '');

FILE_SCHEMA (('AP242_MANAGED_MODEL_BASED_3D_ENGINEERING_MIM_LF { 1 0 10303 442 2 1 4 }'));
ENDSEC;

DATA;
#10=MECHANICAL_DESIGN_GEOMETRIC_PRESENTATION_REPRESENTATION('',(#261),#27807);
#215=SHAPE_REPRESENTATION_RELATIONSHIP('SRR','None',#27912,#237);
#237=ADVANCED_BREP_SHAPE_REPRESENTATION('',(#290),#27792);
#261=STYLED_ITEM('',(#28084),#290);
#290=MANIFOLD_SOLID_BREP('Body1',#12037);
#410=FACE_BOUND('',#2443,.T.);
#411=FACE_BOUND('',#2445,.T.);
#412=FACE_BOUND('',#2447,.T.);
#413=FACE_BOUND('',#2449,.T.);
#639=PLANE('',#13202);
#640=PLANE('',#13203);
#641=PLANE('',#13204);
#642=PLANE('',#13205);
#643=PLANE('',#13206);
#644=PLANE('',#13207);
#1136=CYLINDRICAL_SURFACE('',#13187,3.99999999999999);
#1137=CYLINDRICAL_SURFACE('',#13190,2.99999999999999);
#1138=CYLINDRICAL_SURFACE('',#13193,4.00000000000004);
#1139=CYLINDRICAL_SURFACE('',#13196,2.99999999999999);
#1140=CYLINDRICAL_SURFACE('',#13199,4.00000000000004);
#1664=FACE_OUTER_BOUND('',#2436,.T.);
#1665=FACE_OUTER_BOUND('',#2437,.T.);
#1666=FACE_OUTER_BOUND('',#2438,.T.);
#1667=FACE_OUTER_BOUND('',#2439,.T.);
#1668=FACE_OUTER_BOUND('',#2440,.T.);
#1669=FACE_OUTER_BOUND('',#2441,.T.);
#1670=FACE_OUTER_BOUND('',#2442,.T.);
#1671=FACE_OUTER_BOUND('',#2444,.T.);
#1672=FACE_OUTER_BOUND('',#2446,.T.);
#1673=FACE_OUTER_BOUND('',#2448,.T.);
#1674=FACE_OUTER_BOUND('',#2450,.T.);
#2436=EDGE_LOOP('',(#9961,#9962,#9963,#9964));
#2437=EDGE_LOOP('',(#9965,#9966,#9967,#9968));
#2438=EDGE_LOOP('',(#9969,#9970,#9971,#9972));
#2439=EDGE_LOOP('',(#9973,#9974,#9975,#9976));
#2440=EDGE_LOOP('',(#9977,#9978,#9979,#9980));
#2441=EDGE_LOOP('',(#9981));
#2442=EDGE_LOOP('',(#9982));
#2443=EDGE_LOOP('',(#9983));
#2444=EDGE_LOOP('',(#9984));
#2445=EDGE_LOOP('',(#9985));
#2446=EDGE_LOOP('',(#9986));
#2447=EDGE_LOOP('',(#9987));
#2448=EDGE_LOOP('',(#9988));
#2449=EDGE_LOOP('',(#9989));
#2450=EDGE_LOOP('',(#9990));
#3275=LINE('',#21263,#4095);
#3276=LINE('',#21269,#4096);
#3277=LINE('',#21275,#4097);
#3278=LINE('',#21281,#4098);
#3279=LINE('',#21287,#4099);
#4095=VECTOR('',#16035,3.99999999999999);
#4096=VECTOR('',#16042,2.99999999999999);
#4097=VECTOR('',#16049,4.00000000000004);
#4098=VECTOR('',#16056,2.99999999999999);
#4099=VECTOR('',#16063,4.00000000000004);
#4801=CIRCLE('',#13188,3.99999999999999);
#4802=CIRCLE('',#13189,3.99999999999999);
#4803=CIRCLE('',#13191,2.99999999999999);
#4804=CIRCLE('',#13192,2.99999999999999);
#4805=CIRCLE('',#13194,3.99999999999999);
#4806=CIRCLE('',#13195,4.00000000000003);
#4807=CIRCLE('',#13197,2.99999999999999);
#4808=CIRCLE('',#13198,2.99999999999999);
#4809=CIRCLE('',#13200,4.00000000000003);
#4810=CIRCLE('',#13201,4.00000000000003);
#5714=VERTEX_POINT('',#21260);
#5715=VERTEX_POINT('',#21262);
#5716=VERTEX_POINT('',#21266);
#5717=VERTEX_POINT('',#21268);
#5718=VERTEX_POINT('',#21272);
#5719=VERTEX_POINT('',#21274);
#5720=VERTEX_POINT('',#21278);
#5721=VERTEX_POINT('',#21280);
#5722=VERTEX_POINT('',#21284);
#5723=VERTEX_POINT('',#21286);
#7193=EDGE_CURVE('',#5714,#5714,#4801,.T.);
#7194=EDGE_CURVE('',#5714,#5715,#3275,.T.);
#7195=EDGE_CURVE('',#5715,#5715,#4802,.T.);
#7196=EDGE_CURVE('',#5716,#5716,#4803,.T.);
#7197=EDGE_CURVE('',#5716,#5717,#3276,.T.);
#7198=EDGE_CURVE('',#5717,#5717,#4804,.T.);
#7199=EDGE_CURVE('',#5718,#5718,#4805,.T.);
#7200=EDGE_CURVE('',#5718,#5719,#3277,.T.);
#7201=EDGE_CURVE('',#5719,#5719,#4806,.T.);
#7202=EDGE_CURVE('',#5720,#5720,#4807,.T.);
#7203=EDGE_CURVE('',#5720,#5721,#3278,.T.);
#7204=EDGE_CURVE('',#5721,#5721,#4808,.T.);
#7205=EDGE_CURVE('',#5722,#5722,#4809,.T.);
#7206=EDGE_CURVE('',#5722,#5723,#3279,.T.);
#7207=EDGE_CURVE('',#5723,#5723,#4810,.T.);
#9961=ORIENTED_EDGE('',*,*,#7193,.F.);
#9962=ORIENTED_EDGE('',*,*,#7194,.T.);
#9963=ORIENTED_EDGE('',*,*,#7195,.T.);
#9964=ORIENTED_EDGE('',*,*,#7194,.F.);
#9965=ORIENTED_EDGE('',*,*,#7196,.F.);
#9966=ORIENTED_EDGE('',*,*,#7197,.T.);
#9967=ORIENTED_EDGE('',*,*,#7198,.T.);
#9968=ORIENTED_EDGE('',*,*,#7197,.F.);
#9969=ORIENTED_EDGE('',*,*,#7199,.F.);
#9970=ORIENTED_EDGE('',*,*,#7200,.T.);
#9971=ORIENTED_EDGE('',*,*,#7201,.T.);
#9972=ORIENTED_EDGE('',*,*,#7200,.F.);
#9973=ORIENTED_EDGE('',*,*,#7202,.F.);
#9974=ORIENTED_EDGE('',*,*,#7203,.T.);
#9975=ORIENTED_EDGE('',*,*,#7204,.T.);
#9976=ORIENTED_EDGE('',*,*,#7203,.F.);
#9977=ORIENTED_EDGE('',*,*,#7205,.F.);
#9978=ORIENTED_EDGE('',*,*,#7206,.T.);
#9979=ORIENTED_EDGE('',*,*,#7207,.T.);
#9980=ORIENTED_EDGE('',*,*,#7206,.F.);
#9981=ORIENTED_EDGE('',*,*,#7207,.F.);
#9982=ORIENTED_EDGE('',*,*,#7205,.T.);
#9983=ORIENTED_EDGE('',*,*,#7204,.F.);
#9984=ORIENTED_EDGE('',*,*,#7201,.F.);
#9985=ORIENTED_EDGE('',*,*,#7202,.T.);
#9986=ORIENTED_EDGE('',*,*,#7199,.T.);
#9987=ORIENTED_EDGE('',*,*,#7198,.F.);
#9988=ORIENTED_EDGE('',*,*,#7195,.F.);
#9989=ORIENTED_EDGE('',*,*,#7196,.T.);
#9990=ORIENTED_EDGE('',*,*,#7193,.T.);
#11746=ADVANCED_FACE('',(#1664),#1136,.T.);
#11747=ADVANCED_FACE('',(#1665),#1137,.T.);
#11748=ADVANCED_FACE('',(#1666),#1138,.T.);
#11749=ADVANCED_FACE('',(#1667),#1139,.T.);
#11750=ADVANCED_FACE('',(#1668),#1140,.T.);
#11751=ADVANCED_FACE('',(#1669),#639,.T.);
#11752=ADVANCED_FACE('',(#1670,#410),#640,.T.);
#11753=ADVANCED_FACE('',(#1671,#411),#641,.T.);
#11754=ADVANCED_FACE('',(#1672,#412),#642,.T.);
#11755=ADVANCED_FACE('',(#1673,#413),#643,.T.);
#11756=ADVANCED_FACE('',(#1674),#644,.T.);
#12037=CLOSED_SHELL('',(#11746,#11747,#11748,#11749,#11750,#11751,#11752,
#11753,#11754,#11755,#11756));
#13186=AXIS2_PLACEMENT_3D('',#21258,#16029,#16030);
#13187=AXIS2_PLACEMENT_3D('',#21259,#16031,#16032);
#13188=AXIS2_PLACEMENT_3D('',#21261,#16033,#16034);
#13189=AXIS2_PLACEMENT_3D('',#21264,#16036,#16037);
#13190=AXIS2_PLACEMENT_3D('',#21265,#16038,#16039);
#13191=AXIS2_PLACEMENT_3D('',#21267,#16040,#16041);
#13192=AXIS2_PLACEMENT_3D('',#21270,#16043,#16044);
#13193=AXIS2_PLACEMENT_3D('',#21271,#16045,#16046);
#13194=AXIS2_PLACEMENT_3D('',#21273,#16047,#16048);
#13195=AXIS2_PLACEMENT_3D('',#21276,#16050,#16051);
#13196=AXIS2_PLACEMENT_3D('',#21277,#16052,#16053);
#13197=AXIS2_PLACEMENT_3D('',#21279,#16054,#16055);
#13198=AXIS2_PLACEMENT_3D('',#21282,#16057,#16058);
#13199=AXIS2_PLACEMENT_3D('',#21283,#16059,#16060);
#13200=AXIS2_PLACEMENT_3D('',#21285,#16061,#16062);
#13201=AXIS2_PLACEMENT_3D('',#21288,#16064,#16065);
#13202=AXIS2_PLACEMENT_3D('',#21289,#16066,#16067);
#13203=AXIS2_PLACEMENT_3D('',#21290,#16068,#16069);
#13204=AXIS2_PLACEMENT_3D('',#21291,#16070,#16071);
#13205=AXIS2_PLACEMENT_3D('',#21292,#16072,#16073);
#13206=AXIS2_PLACEMENT_3D('',#21293,#16074,#16075);
#13207=AXIS2_PLACEMENT_3D('',#21294,#16076,#16077);
#16029=DIRECTION('axis',(0.,0.,1.));
#16030=DIRECTION('refdir',(1.,0.,0.));
#16031=DIRECTION('center_axis',(0.224684645967588,0.974431531646231,6.6078080723141E-17));
#16032=DIRECTION('ref_axis',(0.893873580715705,-0.206109575173111,0.398131717802593));
#16033=DIRECTION('center_axis',(0.224684645967588,0.974431531646231,6.6078080723141E-17));
#16034=DIRECTION('ref_axis',(0.893873580715705,-0.206109575173111,0.398131717802593));
#16035=DIRECTION('',(-0.224684645967588,-0.974431531646231,-6.6078080723141E-17));
#16036=DIRECTION('center_axis',(0.224684645967588,0.974431531646231,6.6078080723141E-17));
#16037=DIRECTION('ref_axis',(0.893873580715705,-0.206109575173111,0.398131717802593));
#16038=DIRECTION('center_axis',(0.224684645967588,0.974431531646231,6.6078080723141E-17));
#16039=DIRECTION('ref_axis',(0.893873580715709,-0.206109575173112,0.398131717802583));
#16040=DIRECTION('center_axis',(0.224684645967588,0.974431531646231,6.6078080723141E-17));
#16041=DIRECTION('ref_axis',(0.893873580715709,-0.206109575173112,0.398131717802583));
#16042=DIRECTION('',(-0.224684645967588,-0.974431531646231,-6.6078080723141E-17));
#16043=DIRECTION('center_axis',(0.224684645967588,0.974431531646231,6.6078080723141E-17));
#16044=DIRECTION('ref_axis',(0.893873580715709,-0.206109575173112,0.398131717802583));
#16045=DIRECTION('center_axis',(0.224684645967588,0.974431531646231,6.6078080723141E-17));
#16046=DIRECTION('ref_axis',(0.893873580715707,-0.206109575173112,0.398131717802588));
#16047=DIRECTION('center_axis',(0.224684645967588,0.974431531646231,6.6078080723141E-17));
#16048=DIRECTION('ref_axis',(0.893873580715705,-0.206109575173111,0.398131717802593));
#16049=DIRECTION('',(-0.224684645967588,-0.974431531646231,-6.6078080723141E-17));
#16050=DIRECTION('center_axis',(0.224684645967588,0.974431531646231,6.6078080723141E-17));
#16051=DIRECTION('ref_axis',(0.893873580715707,-0.206109575173112,0.398131717802588));
#16052=DIRECTION('center_axis',(0.224684645967588,0.974431531646231,6.6078080723141E-17));
#16053=DIRECTION('ref_axis',(0.893873580715709,-0.206109575173112,0.398131717802583));
#16054=DIRECTION('center_axis',(0.224684645967588,0.974431531646231,6.6078080723141E-17));
#16055=DIRECTION('ref_axis',(0.893873580715709,-0.206109575173112,0.398131717802583));
#16056=DIRECTION('',(-0.224684645967588,-0.974431531646231,-6.6078080723141E-17));
#16057=DIRECTION('center_axis',(0.224684645967588,0.974431531646231,6.6078080723141E-17));
#16058=DIRECTION('ref_axis',(0.893873580715709,-0.206109575173112,0.398131717802583));
#16059=DIRECTION('center_axis',(0.224684645967588,0.974431531646231,6.6078080723141E-17));
#16060=DIRECTION('ref_axis',(0.893873580715707,-0.206109575173112,0.398131717802588));
#16061=DIRECTION('center_axis',(0.224684645967588,0.974431531646231,6.6078080723141E-17));
#16062=DIRECTION('ref_axis',(0.893873580715707,-0.206109575173112,0.398131717802588));
#16063=DIRECTION('',(-0.224684645967588,-0.974431531646231,-6.6078080723141E-17));
#16064=DIRECTION('center_axis',(0.224684645967588,0.974431531646231,6.6078080723141E-17));
#16065=DIRECTION('ref_axis',(0.893873580715707,-0.206109575173112,0.398131717802588));
#16066=DIRECTION('center_axis',(-0.224684645967588,-0.974431531646231,-2.77555756156289E-17));
#16067=DIRECTION('ref_axis',(-0.893873580715708,0.206109575173112,-0.398131717802585));
#16068=DIRECTION('center_axis',(0.224684645967588,0.974431531646231,2.77555756156289E-17));
#16069=DIRECTION('ref_axis',(0.893873580715708,-0.206109575173112,0.398131717802585));
#16070=DIRECTION('center_axis',(-0.224684645967588,-0.974431531646231,-2.77555756156289E-17));
#16071=DIRECTION('ref_axis',(-0.893873580715708,0.206109575173112,-0.398131717802585));
#16072=DIRECTION('center_axis',(0.224684645967588,0.974431531646231,2.77555756156289E-17));
#16073=DIRECTION('ref_axis',(0.893873580715708,-0.206109575173112,0.398131717802585));
#16074=DIRECTION('center_axis',(-0.224684645967588,-0.974431531646231,-2.77555756156289E-17));
#16075=DIRECTION('ref_axis',(-0.893873580715708,0.206109575173112,-0.398131717802585));
#16076=DIRECTION('center_axis',(0.224684645967588,0.974431531646231,2.77555756156289E-17));
#16077=DIRECTION('ref_axis',(0.893873580715708,-0.206109575173112,0.398131717802585));
#21258=CARTESIAN_POINT('',(0.,0.,0.));
#21259=CARTESIAN_POINT('Origin',(271.986847992623,154.073622192239,260.573593133705));
#21260=CARTESIAN_POINT('',(268.41135366976,154.898060492931,258.981066262494));
#21261=CARTESIAN_POINT('Origin',(271.986847992623,154.073622192239,260.573593133705));
#21262=CARTESIAN_POINT('',(267.624957408873,151.487550132169,258.981066262494));
#21263=CARTESIAN_POINT('',(268.41135366976,154.898060492931,258.981066262494));
#21264=CARTESIAN_POINT('Origin',(271.200451731736,150.663111831477,260.573593133705));
#21265=CARTESIAN_POINT('Origin',(271.986847992623,154.073622192239,260.573593133705));
#21266=CARTESIAN_POINT('',(268.518830989589,151.281440556996,259.379197980297));
#21267=CARTESIAN_POINT('Origin',(271.200451731736,150.663111831477,260.573593133705));
#21268=CARTESIAN_POINT('',(268.181804020638,149.819793259527,259.379197980297));
#21269=CARTESIAN_POINT('',(269.305227250476,154.691950917758,259.379197980297));
#21270=CARTESIAN_POINT('Origin',(270.863424762785,149.201464534007,260.573593133705));
#21271=CARTESIAN_POINT('Origin',(271.986847992623,154.073622192239,260.573593133705));
#21272=CARTESIAN_POINT('',(267.287930439922,150.0259028347,258.981066262494));
#21273=CARTESIAN_POINT('Origin',(270.863424762785,149.201464534007,260.573593133705));
#21274=CARTESIAN_POINT('',(258.974598539121,113.971936163789,258.981066262494));
#21275=CARTESIAN_POINT('',(268.41135366976,154.898060492931,258.981066262494));
#21276=CARTESIAN_POINT('Origin',(262.550092861984,113.147497863097,260.573593133705));
#21277=CARTESIAN_POINT('Origin',(271.986847992623,154.073622192239,260.573593133705));
#21278=CARTESIAN_POINT('',(259.868472119837,113.765826588616,259.379197980297));
#21279=CARTESIAN_POINT('Origin',(262.550092861984,113.147497863097,260.573593133705));
#21280=CARTESIAN_POINT('',(259.419102827902,111.816963525324,259.379197980297));
#21281=CARTESIAN_POINT('',(269.305227250476,154.691950917758,259.379197980297));
#21282=CARTESIAN_POINT('Origin',(262.100723570049,111.198634799804,260.573593133705));
#21283=CARTESIAN_POINT('Origin',(271.986847992623,154.073622192239,260.573593133705));
#21284=CARTESIAN_POINT('',(258.525229247186,112.023073100497,258.981066262494));
#21285=CARTESIAN_POINT('Origin',(262.100723570049,111.198634799804,260.573593133705));
#21286=CARTESIAN_POINT('',(258.300544601218,111.048641568851,258.981066262494));
#21287=CARTESIAN_POINT('',(268.41135366976,154.898060492931,258.981066262494));
#21288=CARTESIAN_POINT('Origin',(261.876038924081,110.224203268158,260.573593133705));
#21289=CARTESIAN_POINT('Origin',(261.876038924081,110.224203268158,260.573593133705));
#21290=CARTESIAN_POINT('Origin',(265.676217892912,110.374196499112,262.166120004915));
#21291=CARTESIAN_POINT('Origin',(265.231713604131,112.529169137578,261.767988287112));
#21292=CARTESIAN_POINT('Origin',(274.438919085648,148.377026233315,262.166120004915));
#21293=CARTESIAN_POINT('Origin',(273.882072473883,150.044783105957,261.767988287112));
#21294=CARTESIAN_POINT('Origin',(275.562342315485,153.249183891546,262.166120004915));
#27763=UNCERTAINTY_MEASURE_WITH_UNIT(LENGTH_MEASURE(0.01),#27808,
'DISTANCE_ACCURACY_VALUE',
'Maximum model space distance between geometric entities at asserted c
onnectivities');
#27778=UNCERTAINTY_MEASURE_WITH_UNIT(LENGTH_MEASURE(0.01),#27808,
'DISTANCE_ACCURACY_VALUE',
'Maximum model space distance between geometric entities at asserted c
onnectivities');
#27792=(
GEOMETRIC_REPRESENTATION_CONTEXT(3)
GLOBAL_UNCERTAINTY_ASSIGNED_CONTEXT((#27763))
GLOBAL_UNIT_ASSIGNED_CONTEXT((#27808,#27810,#27811))
REPRESENTATION_CONTEXT('','3D')
);
#27807=(
GEOMETRIC_REPRESENTATION_CONTEXT(3)
GLOBAL_UNCERTAINTY_ASSIGNED_CONTEXT((#27778))
GLOBAL_UNIT_ASSIGNED_CONTEXT((#27808,#27810,#27811))
REPRESENTATION_CONTEXT('','3D')
);
#27808=(
LENGTH_UNIT()
NAMED_UNIT(*)
SI_UNIT(.MILLI.,.METRE.)
);
#27810=(
NAMED_UNIT(*)
PLANE_ANGLE_UNIT()
SI_UNIT($,.RADIAN.)
);
#27811=(
NAMED_UNIT(*)
SI_UNIT($,.STERADIAN.)
SOLID_ANGLE_UNIT()
);
#27825=SHAPE_DEFINITION_REPRESENTATION(#27858,#27912);
#27858=PRODUCT_DEFINITION_SHAPE('',$,#27941);
#27912=SHAPE_REPRESENTATION('',(#13186),#27792);
#27927=PRODUCT_DEFINITION_CONTEXT('part definition',#28013,'design');
#27941=PRODUCT_DEFINITION('Release Valve Screw','Release Valve Screw',#27969,
#27927);
#27969=PRODUCT_DEFINITION_FORMATION('',$,#28028);
#28013=APPLICATION_CONTEXT('Managed model based 3d engineering');
#28014=PRODUCT_CONTEXT('part definition',#28013,'mechanical');
#28028=PRODUCT('Release Valve Screw','Release Valve Screw',$,(#28014));
#28078=COLOUR_RGB('Black',0.12,0.14,0.17);
#28079=FILL_AREA_STYLE_COLOUR('',#28078);
#28080=FILL_AREA_STYLE('',(#28079));
#28081=SURFACE_STYLE_FILL_AREA(#28080);
#28082=SURFACE_SIDE_STYLE('',(#28081));
#28083=SURFACE_STYLE_USAGE(.BOTH.,#28082);
#28084=PRESENTATION_STYLE_ASSIGNMENT((#28083));
ENDSEC;
END-ISO-10303-21;
